ISO-10303-21;
HEADER;
FILE_DESCRIPTION (('STEP AP214'),
    '1' );
FILE_NAME ('pin.step',
    '2026-10-11T23:18:24',
    ( '' ),
    ( '' ),
    'SwSTEP 2.0',
    'SolidWorks 2021',
    '' );
FILE_SCHEMA (( 'AUTOMOTIVE_DESIGN' ));
ENDSEC;

DATA;
#2=DIRECTION ( 'NONE',  ( 0.000000000000000000, 1.000000000000000000, 0.000000000000000000 ) ) ;
#89=CIRCLE ( 'NONE', #4911, 1.500000000000000222 ) ;
#326=CIRCLE ( 'NONE', #9338, 2.500000000000000000 ) ;
#348=( NAMED_UNIT ( * ) PLANE_ANGLE_UNIT ( ) SI_UNIT ( $, .RADIAN. ) );
#396=FACE_BOUND ( 'NONE', #8897, .T. ) ;
#431=EDGE_LOOP ( 'NONE', ( #8073, #1131 ) ) ;
#494=CIRCLE ( 'NONE', #3132, 2.500000000000000444 ) ;
#507=DIRECTION ( 'NONE',  ( 0.000000000000000000, 0.000000000000000000, 1.000000000000000000 ) ) ;
#570=FACE_OUTER_BOUND ( 'NONE', #4411, .T. ) ;
#581=PRODUCT_DEFINITION_FORMATION_WITH_SPECIFIED_SOURCE ( 'ANY', '', #4340, .NOT_KNOWN. ) ;
#661=DIRECTION ( 'NONE',  ( 0.000000000000000000, 0.000000000000000000, 1.000000000000000000 ) ) ;
#713=APPLICATION_CONTEXT ( 'automotive_design' ) ;
#742=LINE ( 'NONE', #10031, #3726 ) ;
#784=VECTOR ( 'NONE', #13170, 1000.000000000000000 ) ;
#845=CARTESIAN_POINT ( 'NONE',  ( 3.061616997868383141E-16, 14.00000000000000178, 2.500000000000000000 ) ) ;
#892=VECTOR ( 'NONE', #7735, 1000.000000000000000 ) ;
#992=CYLINDRICAL_SURFACE ( 'NONE', #3950, 2.500000000000000000 ) ;
#1003=EDGE_LOOP ( 'NONE', ( #12475, #4348 ) ) ;
#1086=CARTESIAN_POINT ( 'NONE',  ( 3.061616997868383141E-16, 14.00000000000000178, 2.500000000000000000 ) ) ;
#1108=DIRECTION ( 'NONE',  ( 0.000000000000000000, 1.000000000000000000, 0.000000000000000000 ) ) ;
#1121=FACE_OUTER_BOUND ( 'NONE', #431, .T. ) ;
#1131=ORIENTED_EDGE ( 'NONE', *, *, #11631, .F. ) ;
#1164=AXIS2_PLACEMENT_3D ( 'NONE', #7954, #12178, #661 ) ;
#1200=CIRCLE ( 'NONE', #4715, 2.500000000000000444 ) ;
#1315=ORIENTED_EDGE ( 'NONE', *, *, #6400, .F. ) ;
#1334=AXIS2_PLACEMENT_3D ( 'NONE', #11991, #9594, #5316 ) ;
#1381=ADVANCED_FACE ( 'NONE', ( #4755 ), #13486, .T. ) ;
#1496=DIRECTION ( 'NONE',  ( 0.000000000000000000, 1.000000000000000000, 0.000000000000000000 ) ) ;
#1506=SURFACE_STYLE_FILL_AREA ( #6798 ) ;
#1579=DIRECTION ( 'NONE',  ( 0.000000000000000000, 0.000000000000000000, 1.000000000000000000 ) ) ;
#1611=AXIS2_PLACEMENT_3D ( 'NONE', #2050, #7158, #8369 ) ;
#1946=ADVANCED_FACE ( 'NONE', ( #13059 ), #3617, .T. ) ;
#1993=EDGE_CURVE ( 'NONE', #12500, #12757, #7554, .T. ) ;
#2031=ORIENTED_EDGE ( 'NONE', *, *, #8422, .F. ) ;
#2050=CARTESIAN_POINT ( 'NONE',  ( 0.000000000000000000, 14.00000000000000178, 0.000000000000000000 ) ) ;
#2067=ORIENTED_EDGE ( 'NONE', *, *, #3148, .F. ) ;
#2117=ORIENTED_EDGE ( 'NONE', *, *, #10374, .T. ) ;
#2368=ORIENTED_EDGE ( 'NONE', *, *, #5983, .F. ) ;
#2410=ORIENTED_EDGE ( 'NONE', *, *, #4844, .F. ) ;
#2411=ORIENTED_EDGE ( 'NONE', *, *, #8154, .T. ) ;
#2507=CARTESIAN_POINT ( 'NONE',  ( 0.000000000000000000, 13.00000000000000178, 0.000000000000000000 ) ) ;
#2543=( NAMED_UNIT ( * ) PLANE_ANGLE_UNIT ( ) SI_UNIT ( $, .RADIAN. ) );
#2587=CARTESIAN_POINT ( 'NONE',  ( 0.000000000000000000, 13.00000000000000178, 0.000000000000000000 ) ) ;
#2593=CARTESIAN_POINT ( 'NONE',  ( 0.000000000000000000, 14.00000000000000178, -2.500000000000000000 ) ) ;
#2605=CARTESIAN_POINT ( 'NONE',  ( 3.061616997868383634E-16, 1.000000000000000000, 2.500000000000000444 ) ) ;
#2610=VERTEX_POINT ( 'NONE', #8403 ) ;
#2638=DIRECTION ( 'NONE',  ( -0.000000000000000000, -1.000000000000000000, -0.000000000000000000 ) ) ;
#2650=AXIS2_PLACEMENT_3D ( 'NONE', #8607, #12835, #1579 ) ;
#2705=DIRECTION ( 'NONE',  ( 0.000000000000000000, 1.000000000000000000, 0.000000000000000000 ) ) ;
#2710=DIRECTION ( 'NONE',  ( 0.000000000000000000, 1.000000000000000000, 0.000000000000000000 ) ) ;
#2727=CYLINDRICAL_SURFACE ( 'NONE', #10629, 1.500000000000000222 ) ;
#2763=CARTESIAN_POINT ( 'NONE',  ( 0.000000000000000000, 14.00000000000000178, 0.000000000000000000 ) ) ;
#2818=PRODUCT_DEFINITION_CONTEXT ( 'detailed design', #5544, 'design' ) ;
#2828=FACE_OUTER_BOUND ( 'NONE', #6907, .T. ) ;
#2967=CIRCLE ( 'NONE', #6264, 2.500000000000000000 ) ;
#2987=STYLED_ITEM ( 'NONE', ( #3493 ), #12787 ) ;
#3032=DIRECTION ( 'NONE',  ( 0.000000000000000000, 0.000000000000000000, -1.000000000000000000 ) ) ;
#3086=VERTEX_POINT ( 'NONE', #11986 ) ;
#3132=AXIS2_PLACEMENT_3D ( 'NONE', #8812, #10966, #10068 ) ;
#3148=EDGE_CURVE ( 'NONE', #11517, #2610, #13081, .T. ) ;
#3361=SURFACE_SIDE_STYLE ('',( #1506 ) ) ;
#3381=DIRECTION ( 'NONE',  ( 0.000000000000000000, 0.000000000000000000, 1.000000000000000000 ) ) ;
#3428=FILL_AREA_STYLE_COLOUR ( '', #7392 ) ;
#3458=VERTEX_POINT ( 'NONE', #10383 ) ;
#3493=PRESENTATION_STYLE_ASSIGNMENT (( #13082 ) ) ;
#3515=FACE_OUTER_BOUND ( 'NONE', #5290, .T. ) ;
#3549=CARTESIAN_POINT ( 'NONE',  ( 0.000000000000000000, 0.000000000000000000, 0.000000000000000000 ) ) ;
#3575=ORIENTED_EDGE ( 'NONE', *, *, #12017, .T. ) ;
#3585=AXIS2_PLACEMENT_3D ( 'NONE', #7025, #2, #6257 ) ;
#3596=VERTEX_POINT ( 'NONE', #5474 ) ;
#3617=CYLINDRICAL_SURFACE ( 'NONE', #11074, 1.500000000000000222 ) ;
#3627=ADVANCED_FACE ( 'NONE', ( #11254 ), #992, .T. ) ;
#3726=VECTOR ( 'NONE', #3754, 1000.000000000000000 ) ;
#3754=DIRECTION ( 'NONE',  ( -0.000000000000000000, -1.000000000000000000, -0.000000000000000000 ) ) ;
#3760=VECTOR ( 'NONE', #2638, 1000.000000000000000 ) ;
#3804=CIRCLE ( 'NONE', #11511, 2.500000000000000444 ) ;
#3889=ORIENTED_EDGE ( 'NONE', *, *, #5409, .T. ) ;
#3896=CARTESIAN_POINT ( 'NONE',  ( 0.000000000000000000, 14.00000000000000178, 0.000000000000000000 ) ) ;
#3950=AXIS2_PLACEMENT_3D ( 'NONE', #12301, #4088, #12510 ) ;
#4063=ADVANCED_FACE ( 'NONE', ( #2828 ), #4070, .T. ) ;
#4070=CYLINDRICAL_SURFACE ( 'NONE', #12344, 2.500000000000000444 ) ;
#4088=DIRECTION ( 'NONE',  ( -0.000000000000000000, -1.000000000000000000, -0.000000000000000000 ) ) ;
#4173=EDGE_LOOP ( 'NONE', ( #11072, #8000, #7691, #2410 ) ) ;
#4192=CIRCLE ( 'NONE', #2650, 1.500000000000000222 ) ;
#4251=DIRECTION ( 'NONE',  ( 0.000000000000000000, 1.000000000000000000, 0.000000000000000000 ) ) ;
#4279=ORIENTED_EDGE ( 'NONE', *, *, #5730, .F. ) ;
#4289=PRODUCT_DEFINITION ( 'UNKNOWN', '', #581, #2818 ) ;
#4340=PRODUCT ( 'pin', 'pin', '', ( #13494 ) ) ;
#4348=ORIENTED_EDGE ( 'NONE', *, *, #10030, .T. ) ;
#4385=VECTOR ( 'NONE', #8788, 1000.000000000000000 ) ;
#4411=EDGE_LOOP ( 'NONE', ( #12133, #5226 ) ) ;
#4422=DIRECTION ( 'NONE',  ( 0.000000000000000000, 0.000000000000000000, -1.000000000000000000 ) ) ;
#4435=AXIS2_PLACEMENT_3D ( 'NONE', #6626, #11936, #4422 ) ;
#4466=SHAPE_REPRESENTATION_RELATIONSHIP ( 'NONE' , 'NONE' ,  #8461, #12787 ) ;
#4475=MECHANICAL_DESIGN_GEOMETRIC_PRESENTATION_REPRESENTATION('',(#9093),#11743);
#4630=CIRCLE ( 'NONE', #7704, 2.500000000000000000 ) ;
#4658=DIRECTION ( 'NONE',  ( 0.000000000000000000, 1.000000000000000000, 0.000000000000000000 ) ) ;
#4684=CIRCLE ( 'NONE', #1164, 2.500000000000000444 ) ;
#4715=AXIS2_PLACEMENT_3D ( 'NONE', #3549, #4658, #10864 ) ;
#4755=FACE_OUTER_BOUND ( 'NONE', #4173, .T. ) ;
#4758=UNCERTAINTY_MEASURE_WITH_UNIT (LENGTH_MEASURE( 1.000000000000000082E-05 ), #13009, 'distance_accuracy_value', 'NONE');
#4784=LINE ( 'NONE', #4846, #3760 ) ;
#4844=EDGE_CURVE ( 'NONE', #12757, #3458, #742, .T. ) ;
#4846=CARTESIAN_POINT ( 'NONE',  ( 0.000000000000000000, 1.000000000000000000, -2.500000000000000444 ) ) ;
#4911=AXIS2_PLACEMENT_3D ( 'NONE', #11918, #1108, #8531 ) ;
#5036=DIRECTION ( 'NONE',  ( -0.000000000000000000, -1.000000000000000000, -0.000000000000000000 ) ) ;
#5040=ORIENTED_EDGE ( 'NONE', *, *, #3148, .T. ) ;
#5191=( GEOMETRIC_REPRESENTATION_CONTEXT ( 3 ) GLOBAL_UNCERTAINTY_ASSIGNED_CONTEXT ( ( #10117 ) ) GLOBAL_UNIT_ASSIGNED_CONTEXT ( ( #12492, #2543, #5492 ) ) REPRESENTATION_CONTEXT ( 'NONE', 'WORKASPACE' ) );
#5226=ORIENTED_EDGE ( 'NONE', *, *, #1993, .T. ) ;
#5290=EDGE_LOOP ( 'NONE', ( #13092, #3889, #9582, #12281 ) ) ;
#5295=AXIS2_PLACEMENT_3D ( 'NONE', #6301, #7412, #10513 ) ;
#5316=DIRECTION ( 'NONE',  ( 0.000000000000000000, -0.000000000000000000, 1.000000000000000000 ) ) ;
#5357=( LENGTH_UNIT ( ) NAMED_UNIT ( * ) SI_UNIT ( .MILLI., .METRE. ) );
#5409=EDGE_CURVE ( 'NONE', #11196, #3086, #9037, .T. ) ;
#5429=PRODUCT_DEFINITION_SHAPE ( 'NONE', 'NONE',  #4289 ) ;
#5440=VERTEX_POINT ( 'NONE', #9116 ) ;
#5474=CARTESIAN_POINT ( 'NONE',  ( 0.000000000000000000, 1.000000000000000000, -2.500000000000000444 ) ) ;
#5485=ORIENTED_EDGE ( 'NONE', *, *, #10374, .F. ) ;
#5492=( NAMED_UNIT ( * ) SI_UNIT ( $, .STERADIAN. ) SOLID_ANGLE_UNIT ( ) );
#5537=CLOSED_SHELL ( 'NONE', ( #1381, #1946, #6817, #4063, #8678, #5745, #9945, #3627, #9611, #12754 ) ) ;
#5544=APPLICATION_CONTEXT ( 'automotive_design' ) ;
#5582=ORIENTED_EDGE ( 'NONE', *, *, #10121, .F. ) ;
#5712=DIRECTION ( 'NONE',  ( 1.000000000000000000, 0.000000000000000000, 0.000000000000000000 ) ) ;
#5730=EDGE_CURVE ( 'NONE', #2610, #12350, #4192, .T. ) ;
#5745=ADVANCED_FACE ( 'NONE', ( #1121 ), #10944, .F. ) ;
#5784=EDGE_LOOP ( 'NONE', ( #5821, #8382, #5040, #7788 ) ) ;
#5821=ORIENTED_EDGE ( 'NONE', *, *, #12017, .F. ) ;
#5946=CARTESIAN_POINT ( 'NONE',  ( 3.061616997868383634E-16, 1.000000000000000000, 2.500000000000000444 ) ) ;
#5983=EDGE_CURVE ( 'NONE', #5440, #3458, #4630, .T. ) ;
#6257=DIRECTION ( 'NONE',  ( 0.000000000000000000, -0.000000000000000000, 1.000000000000000000 ) ) ;
#6264=AXIS2_PLACEMENT_3D ( 'NONE', #2507, #2705, #507 ) ;
#6301=CARTESIAN_POINT ( 'NONE',  ( 0.000000000000000000, 13.00000000000000178, 0.000000000000000000 ) ) ;
#6305=ORIENTED_EDGE ( 'NONE', *, *, #13327, .F. ) ;
#6314=SHAPE_DEFINITION_REPRESENTATION ( #5429, #8461 ) ;
#6400=EDGE_CURVE ( 'NONE', #6431, #11517, #8378, .T. ) ;
#6426=ORIENTED_EDGE ( 'NONE', *, *, #4844, .T. ) ;
#6431=VERTEX_POINT ( 'NONE', #10915 ) ;
#6455=CIRCLE ( 'NONE', #11955, 1.500000000000000222 ) ;
#6599=EDGE_CURVE ( 'NONE', #3596, #12785, #4784, .T. ) ;
#6626=CARTESIAN_POINT ( 'NONE',  ( 0.000000000000000000, 1.000000000000000000, 0.000000000000000000 ) ) ;
#6644=ORIENTED_EDGE ( 'NONE', *, *, #8508, .T. ) ;
#6754=CARTESIAN_POINT ( 'NONE',  ( 0.000000000000000000, 0.000000000000000000, 0.000000000000000000 ) ) ;
#6782=DIRECTION ( 'NONE',  ( -0.000000000000000000, -1.000000000000000000, -0.000000000000000000 ) ) ;
#6788=FACE_OUTER_BOUND ( 'NONE', #8532, .T. ) ;
#6798=FILL_AREA_STYLE ('',( #3428 ) ) ;
#6817=ADVANCED_FACE ( 'NONE', ( #3515 ), #11800, .T. ) ;
#6907=EDGE_LOOP ( 'NONE', ( #13281, #5582, #9219, #2411 ) ) ;
#6915=DIRECTION ( 'NONE',  ( 0.000000000000000000, 0.000000000000000000, 1.000000000000000000 ) ) ;
#6989=CARTESIAN_POINT ( 'NONE',  ( 0.000000000000000000, 1.000000000000000000, 0.000000000000000000 ) ) ;
#7025=CARTESIAN_POINT ( 'NONE',  ( 0.000000000000000000, 1.000000000000000000, 0.000000000000000000 ) ) ;
#7036=DIRECTION ( 'NONE',  ( -0.000000000000000000, -1.000000000000000000, -0.000000000000000000 ) ) ;
#7158=DIRECTION ( 'NONE',  ( -0.000000000000000000, -1.000000000000000000, -0.000000000000000000 ) ) ;
#7392=COLOUR_RGB ( '',0.7803921568627451011, 0.7607843137254901578, 0.7411764705882353255 ) ;
#7412=DIRECTION ( 'NONE',  ( 0.000000000000000000, 1.000000000000000000, 0.000000000000000000 ) ) ;
#7473=DIRECTION ( 'NONE',  ( 0.000000000000000000, 1.000000000000000000, 0.000000000000000000 ) ) ;
#7554=CIRCLE ( 'NONE', #7562, 2.500000000000000000 ) ;
#7562=AXIS2_PLACEMENT_3D ( 'NONE', #10303, #10509, #8295 ) ;
#7691=ORIENTED_EDGE ( 'NONE', *, *, #5983, .T. ) ;
#7704=AXIS2_PLACEMENT_3D ( 'NONE', #11424, #4251, #8447 ) ;
#7735=DIRECTION ( 'NONE',  ( -0.000000000000000000, -1.000000000000000000, -0.000000000000000000 ) ) ;
#7788=ORIENTED_EDGE ( 'NONE', *, *, #5730, .T. ) ;
#7851=PLANE ( 'NONE',  #12171 ) ;
#7954=CARTESIAN_POINT ( 'NONE',  ( 0.000000000000000000, 1.000000000000000000, 0.000000000000000000 ) ) ;
#8000=ORIENTED_EDGE ( 'NONE', *, *, #8422, .T. ) ;
#8073=ORIENTED_EDGE ( 'NONE', *, *, #8154, .F. ) ;
#8154=EDGE_CURVE ( 'NONE', #12785, #3086, #494, .T. ) ;
#8244=EDGE_LOOP ( 'NONE', ( #2031, #9729, #6426, #10950 ) ) ;
#8266=CARTESIAN_POINT ( 'NONE',  ( 0.000000000000000000, 1.000000000000000000, 0.000000000000000000 ) ) ;
#8295=DIRECTION ( 'NONE',  ( 0.000000000000000000, 0.000000000000000000, 1.000000000000000000 ) ) ;
#8369=DIRECTION ( 'NONE',  ( 0.000000000000000000, 0.000000000000000000, -1.000000000000000000 ) ) ;
#8378=CIRCLE ( 'NONE', #5295, 1.500000000000000222 ) ;
#8382=ORIENTED_EDGE ( 'NONE', *, *, #8508, .F. ) ;
#8403=CARTESIAN_POINT ( 'NONE',  ( 0.000000000000000000, 1.000000000000000000, -1.500000000000000222 ) ) ;
#8422=EDGE_CURVE ( 'NONE', #12500, #5440, #11318, .T. ) ;
#8447=DIRECTION ( 'NONE',  ( 0.000000000000000000, 0.000000000000000000, 1.000000000000000000 ) ) ;
#8461=SHAPE_REPRESENTATION ( 'pin', ( #10007 ), #5191 ) ;
#8508=EDGE_CURVE ( 'NONE', #11517, #6431, #89, .T. ) ;
#8531=DIRECTION ( 'NONE',  ( 0.000000000000000000, 0.000000000000000000, 1.000000000000000000 ) ) ;
#8532=EDGE_LOOP ( 'NONE', ( #6305, #2368 ) ) ;
#8607=CARTESIAN_POINT ( 'NONE',  ( 0.000000000000000000, 1.000000000000000000, 0.000000000000000000 ) ) ;
#8678=ADVANCED_FACE ( 'NONE', ( #9423, #11368 ), #9156, .T. ) ;
#8742=ORIENTED_EDGE ( 'NONE', *, *, #6400, .T. ) ;
#8788=DIRECTION ( 'NONE',  ( -0.000000000000000000, -1.000000000000000000, -0.000000000000000000 ) ) ;
#8812=CARTESIAN_POINT ( 'NONE',  ( 0.000000000000000000, 0.000000000000000000, 0.000000000000000000 ) ) ;
#8836=MANIFOLD_SOLID_BREP ( 'Boss-Extrude3', #5537 ) ;
#8885=DIRECTION ( 'NONE',  ( 0.000000000000000000, -0.000000000000000000, 1.000000000000000000 ) ) ;
#8897=EDGE_LOOP ( 'NONE', ( #6644, #8742 ) ) ;
#8955=CARTESIAN_POINT ( 'NONE',  ( 1.836970198721030181E-16, 13.00000000000000178, 1.500000000000000222 ) ) ;
#9037=LINE ( 'NONE', #5946, #892 ) ;
#9093=STYLED_ITEM('',(#13649),#8836);
#9116=CARTESIAN_POINT ( 'NONE',  ( 3.061616997868383141E-16, 13.00000000000000178, 2.500000000000000000 ) ) ;
#9132=DIRECTION ( 'NONE',  ( 0.000000000000000000, 0.000000000000000000, -1.000000000000000000 ) ) ;
#9156=PLANE ( 'NONE',  #3585 ) ;
#9219=ORIENTED_EDGE ( 'NONE', *, *, #6599, .T. ) ;
#9269=DIRECTION ( 'NONE',  ( 0.000000000000000000, 0.000000000000000000, 1.000000000000000000 ) ) ;
#9338=AXIS2_PLACEMENT_3D ( 'NONE', #3896, #12323, #9269 ) ;
#9341=CARTESIAN_POINT ( 'NONE',  ( 0.000000000000000000, 1.000000000000000000, 0.000000000000000000 ) ) ;
#9423=FACE_BOUND ( 'NONE', #12544, .T. ) ;
#9582=ORIENTED_EDGE ( 'NONE', *, *, #11631, .T. ) ;
#9594=DIRECTION ( 'NONE',  ( 0.000000000000000000, 1.000000000000000000, 0.000000000000000000 ) ) ;
#9611=ADVANCED_FACE ( 'NONE', ( #570 ), #7851, .T. ) ;
#9729=ORIENTED_EDGE ( 'NONE', *, *, #12851, .F. ) ;
#9945=ADVANCED_FACE ( 'NONE', ( #10305 ), #2727, .T. ) ;
#9970=CARTESIAN_POINT ( 'NONE',  ( 0.000000000000000000, 13.00000000000000178, -1.500000000000000222 ) ) ;
#10007=AXIS2_PLACEMENT_3D ( 'NONE', #6754, #3381, #5712 ) ;
#10030=EDGE_CURVE ( 'NONE', #11196, #3596, #4684, .T. ) ;
#10031=CARTESIAN_POINT ( 'NONE',  ( 0.000000000000000000, 14.00000000000000178, -2.500000000000000000 ) ) ;
#10068=DIRECTION ( 'NONE',  ( 0.000000000000000000, 0.000000000000000000, 1.000000000000000000 ) ) ;
#10117=UNCERTAINTY_MEASURE_WITH_UNIT (LENGTH_MEASURE( 1.000000000000000082E-05 ), #12492, 'distance_accuracy_value', 'NONE');
#10121=EDGE_CURVE ( 'NONE', #3596, #11196, #3804, .T. ) ;
#10303=CARTESIAN_POINT ( 'NONE',  ( 0.000000000000000000, 14.00000000000000178, 0.000000000000000000 ) ) ;
#10305=FACE_OUTER_BOUND ( 'NONE', #5784, .T. ) ;
#10374=EDGE_CURVE ( 'NONE', #12350, #2610, #6455, .T. ) ;
#10383=CARTESIAN_POINT ( 'NONE',  ( 0.000000000000000000, 13.00000000000000178, -2.500000000000000000 ) ) ;
#10509=DIRECTION ( 'NONE',  ( 0.000000000000000000, 1.000000000000000000, 0.000000000000000000 ) ) ;
#10513=DIRECTION ( 'NONE',  ( 0.000000000000000000, 0.000000000000000000, 1.000000000000000000 ) ) ;
#10629=AXIS2_PLACEMENT_3D ( 'NONE', #13407, #12253, #11347 ) ;
#10788=CARTESIAN_POINT ( 'NONE',  ( 0.000000000000000000, 13.00000000000000178, -1.500000000000000222 ) ) ;
#10864=DIRECTION ( 'NONE',  ( 0.000000000000000000, 0.000000000000000000, 1.000000000000000000 ) ) ;
#10915=CARTESIAN_POINT ( 'NONE',  ( 1.836970198721030181E-16, 13.00000000000000178, 1.500000000000000222 ) ) ;
#10929=PLANE ( 'NONE',  #12642 ) ;
#10930=( NAMED_UNIT ( * ) PLANE_ANGLE_UNIT ( ) SI_UNIT ( $, .RADIAN. ) );
#10941=( NAMED_UNIT ( * ) SI_UNIT ( $, .STERADIAN. ) SOLID_ANGLE_UNIT ( ) );
#10944=PLANE ( 'NONE',  #1334 ) ;
#10950=ORIENTED_EDGE ( 'NONE', *, *, #13327, .T. ) ;
#10966=DIRECTION ( 'NONE',  ( 0.000000000000000000, 1.000000000000000000, 0.000000000000000000 ) ) ;
#10994=CARTESIAN_POINT ( 'NONE',  ( 0.000000000000000000, 13.00000000000000178, 0.000000000000000000 ) ) ;
#11028=LINE ( 'NONE', #8955, #784 ) ;
#11072=ORIENTED_EDGE ( 'NONE', *, *, #1993, .F. ) ;
#11074=AXIS2_PLACEMENT_3D ( 'NONE', #2587, #6782, #9132 ) ;
#11142=( NAMED_UNIT ( * ) SI_UNIT ( $, .STERADIAN. ) SOLID_ANGLE_UNIT ( ) );
#11193=EDGE_LOOP ( 'NONE', ( #1315, #3575, #2117, #2067 ) ) ;
#11196=VERTEX_POINT ( 'NONE', #2605 ) ;
#11202=CARTESIAN_POINT ( 'NONE',  ( 0.000000000000000000, 0.000000000000000000, -2.500000000000000444 ) ) ;
#11254=FACE_OUTER_BOUND ( 'NONE', #8244, .T. ) ;
#11318=LINE ( 'NONE', #845, #12831 ) ;
#11347=DIRECTION ( 'NONE',  ( 0.000000000000000000, 0.000000000000000000, -1.000000000000000000 ) ) ;
#11350=( GEOMETRIC_REPRESENTATION_CONTEXT ( 3 ) GLOBAL_UNCERTAINTY_ASSIGNED_CONTEXT ( ( #4758 ) ) GLOBAL_UNIT_ASSIGNED_CONTEXT ( ( #13009, #348, #10941 ) ) REPRESENTATION_CONTEXT ( 'NONE', 'WORKASPACE' ) );
#11368=FACE_OUTER_BOUND ( 'NONE', #1003, .T. ) ;
#11424=CARTESIAN_POINT ( 'NONE',  ( 0.000000000000000000, 13.00000000000000178, 0.000000000000000000 ) ) ;
#11474=DIRECTION ( 'NONE',  ( 0.000000000000000000, 0.000000000000000000, 1.000000000000000000 ) ) ;
#11511=AXIS2_PLACEMENT_3D ( 'NONE', #9341, #7473, #11474 ) ;
#11517=VERTEX_POINT ( 'NONE', #10788 ) ;
#11631=EDGE_CURVE ( 'NONE', #3086, #12785, #1200, .T. ) ;
#11743=( GEOMETRIC_REPRESENTATION_CONTEXT ( 3 ) GLOBAL_UNCERTAINTY_ASSIGNED_CONTEXT ( ( #13433 ) ) GLOBAL_UNIT_ASSIGNED_CONTEXT ( ( #5357, #10930, #11142 ) ) REPRESENTATION_CONTEXT ( 'NONE', 'WORKASPACE' ) );
#11800=CYLINDRICAL_SURFACE ( 'NONE', #4435, 2.500000000000000444 ) ;
#11918=CARTESIAN_POINT ( 'NONE',  ( 0.000000000000000000, 13.00000000000000178, 0.000000000000000000 ) ) ;
#11936=DIRECTION ( 'NONE',  ( -0.000000000000000000, -1.000000000000000000, -0.000000000000000000 ) ) ;
#11955=AXIS2_PLACEMENT_3D ( 'NONE', #6989, #2710, #6915 ) ;
#11986=CARTESIAN_POINT ( 'NONE',  ( 3.061616997868383634E-16, 0.000000000000000000, 2.500000000000000444 ) ) ;
#11991=CARTESIAN_POINT ( 'NONE',  ( 0.000000000000000000, 0.000000000000000000, 0.000000000000000000 ) ) ;
#12017=EDGE_CURVE ( 'NONE', #6431, #12350, #11028, .T. ) ;
#12057=CARTESIAN_POINT ( 'NONE',  ( 1.836970198721030181E-16, 1.000000000000000000, 1.500000000000000222 ) ) ;
#12133=ORIENTED_EDGE ( 'NONE', *, *, #12851, .T. ) ;
#12140=DIRECTION ( 'NONE',  ( 0.000000000000000000, 1.000000000000000000, 0.000000000000000000 ) ) ;
#12171=AXIS2_PLACEMENT_3D ( 'NONE', #2763, #12140, #8885 ) ;
#12178=DIRECTION ( 'NONE',  ( 0.000000000000000000, 1.000000000000000000, 0.000000000000000000 ) ) ;
#12184=DIRECTION ( 'NONE',  ( 0.000000000000000000, -0.000000000000000000, 1.000000000000000000 ) ) ;
#12253=DIRECTION ( 'NONE',  ( -0.000000000000000000, -1.000000000000000000, -0.000000000000000000 ) ) ;
#12281=ORIENTED_EDGE ( 'NONE', *, *, #6599, .F. ) ;
#12301=CARTESIAN_POINT ( 'NONE',  ( 0.000000000000000000, 14.00000000000000178, 0.000000000000000000 ) ) ;
#12323=DIRECTION ( 'NONE',  ( 0.000000000000000000, 1.000000000000000000, 0.000000000000000000 ) ) ;
#12344=AXIS2_PLACEMENT_3D ( 'NONE', #8266, #7036, #3032 ) ;
#12350=VERTEX_POINT ( 'NONE', #12057 ) ;
#12475=ORIENTED_EDGE ( 'NONE', *, *, #10121, .T. ) ;
#12492=( LENGTH_UNIT ( ) NAMED_UNIT ( * ) SI_UNIT ( .MILLI., .METRE. ) );
#12500=VERTEX_POINT ( 'NONE', #1086 ) ;
#12510=DIRECTION ( 'NONE',  ( 0.000000000000000000, 0.000000000000000000, -1.000000000000000000 ) ) ;
#12544=EDGE_LOOP ( 'NONE', ( #4279, #5485 ) ) ;
#12642=AXIS2_PLACEMENT_3D ( 'NONE', #10994, #1496, #12184 ) ;
#12668=MECHANICAL_DESIGN_GEOMETRIC_PRESENTATION_REPRESENTATION('',(#2987),#11350);
#12754=ADVANCED_FACE ( 'NONE', ( #396, #6788 ), #10929, .F. ) ;
#12757=VERTEX_POINT ( 'NONE', #2593 ) ;
#12785=VERTEX_POINT ( 'NONE', #11202 ) ;
#12787=ADVANCED_BREP_SHAPE_REPRESENTATION ( '', ( #8836, #10007 ), #5191 ) ;
#12831=VECTOR ( 'NONE', #5036, 1000.000000000000000 ) ;
#12835=DIRECTION ( 'NONE',  ( 0.000000000000000000, 1.000000000000000000, 0.000000000000000000 ) ) ;
#12851=EDGE_CURVE ( 'NONE', #12757, #12500, #326, .T. ) ;
#13009=( LENGTH_UNIT ( ) NAMED_UNIT ( * ) SI_UNIT ( .MILLI., .METRE. ) );
#13059=FACE_OUTER_BOUND ( 'NONE', #11193, .T. ) ;
#13081=LINE ( 'NONE', #9970, #4385 ) ;
#13082=SURFACE_STYLE_USAGE ( .BOTH. , #3361 ) ;
#13092=ORIENTED_EDGE ( 'NONE', *, *, #10030, .F. ) ;
#13170=DIRECTION ( 'NONE',  ( -0.000000000000000000, -1.000000000000000000, -0.000000000000000000 ) ) ;
#13281=ORIENTED_EDGE ( 'NONE', *, *, #5409, .F. ) ;
#13327=EDGE_CURVE ( 'NONE', #3458, #5440, #2967, .T. ) ;
#13407=CARTESIAN_POINT ( 'NONE',  ( 0.000000000000000000, 13.00000000000000178, 0.000000000000000000 ) ) ;
#13433=UNCERTAINTY_MEASURE_WITH_UNIT (LENGTH_MEASURE( 1.000000000000000082E-05 ), #5357, 'distance_accuracy_value', 'NONE');
#13486=CYLINDRICAL_SURFACE ( 'NONE', #1611, 2.500000000000000000 ) ;
#13494=PRODUCT_CONTEXT ( 'NONE', #713, 'mechanical' ) ;
#13643=COLOUR_RGB('Grey',0.48,0.52,0.57);
#13644=FILL_AREA_STYLE_COLOUR('',#13643);
#13645=FILL_AREA_STYLE('',(#13644));
#13646=SURFACE_STYLE_FILL_AREA(#13645);
#13647=SURFACE_SIDE_STYLE('',(#13646));
#13648=SURFACE_STYLE_USAGE(.BOTH.,#13647);
#13649=PRESENTATION_STYLE_ASSIGNMENT((#13648));
ENDSEC;
END-ISO-10303-21;
